ISO-10303-21;
HEADER;
FILE_DESCRIPTION (('STEP AP214'),
    '1' );
FILE_NAME ('slotted pan head screw_iso_ISO 1580 - M2 x 10 - 10N.step',
    '2026-10-27T04:40:18',
    ( '' ),
    ( '' ),
    'SwSTEP 2.0',
    'SolidWorks 2026',
    '' );
FILE_SCHEMA (( 'AUTOMOTIVE_DESIGN' ));
ENDSEC;

DATA;
#22=SHAPE_REPRESENTATION_RELATIONSHIP ( 'NONE' , 'NONE' ,  #8867, #2558 ) ;
#25=DIRECTION ( 'NONE',  ( -1.000000000000000000, -0.000000000000000000, -0.000000000000000000 ) ) ;
#60=DIRECTION ( 'NONE',  ( -1.000000000000000000, -0.000000000000000000, -0.000000000000000000 ) ) ;
#90=CARTESIAN_POINT ( 'NONE',  ( 11.30000000000000426, 1.224646799147353207E-16, -1.000000000000000000 ) ) ;
#130=VECTOR ( 'NONE', #9095, 1000.000000000000000 ) ;
#169=PLANE ( 'NONE',  #3525 ) ;
#215=B_SPLINE_CURVE_WITH_KNOTS ( 'NONE', 3,
 ( #10711, #8988, #7212, #4753, #3985, #5646 ),
 .UNSPECIFIED., .F., .F.,
 ( 4, 2, 4 ),
 ( 0.0005861251363949651497, 0.001008091297609326311, 0.001430057458823687363 ),
 .UNSPECIFIED. ) ;
#227=FACE_OUTER_BOUND ( 'NONE', #9637, .T. ) ;
#230=ORIENTED_EDGE ( 'NONE', *, *, #4677, .T. ) ;
#259=ORIENTED_EDGE ( 'NONE', *, *, #9835, .T. ) ;
#271=ORIENTED_EDGE ( 'NONE', *, *, #9771, .F. ) ;
#279=CARTESIAN_POINT ( 'NONE',  ( 0.3609765494018739029, 0.2499999999999997780, 1.888098105530058968 ) ) ;
#292=VERTEX_POINT ( 'NONE', #997 ) ;
#322=CARTESIAN_POINT ( 'NONE',  ( 0.000000000000000000, 0.000000000000000000, 0.000000000000000000 ) ) ;
#344=CARTESIAN_POINT ( 'NONE',  ( 0.3612935698783895644, -0.2499999999999997224, -1.888152147991466023 ) ) ;
#387=CARTESIAN_POINT ( 'NONE',  ( 1.299999999999999156, 0.000000000000000000, 0.000000000000000000 ) ) ;
#396=DIRECTION ( 'NONE',  ( -1.000000000000000000, -0.000000000000000000, -0.000000000000000000 ) ) ;
#423=DIRECTION ( 'NONE',  ( 1.000000000000000000, 0.000000000000000000, 0.000000000000000000 ) ) ;
#449=DIRECTION ( 'NONE',  ( 0.000000000000000000, 0.000000000000000000, 1.000000000000000000 ) ) ;
#453=DIRECTION ( 'NONE',  ( -1.000000000000000000, 0.000000000000000000, -0.000000000000000000 ) ) ;
#520=AXIS2_PLACEMENT_3D ( 'NONE', #5380, #396, #3722 ) ;
#587=ORIENTED_EDGE ( 'NONE', *, *, #4211, .T. ) ;
#588=DIRECTION ( 'NONE',  ( 1.000000000000000000, 0.000000000000000000, 0.000000000000000000 ) ) ;
#615=EDGE_LOOP ( 'NONE', ( #230, #259, #4915, #1418 ) ) ;
#694=EDGE_LOOP ( 'NONE', ( #1478, #1766 ) ) ;
#724=VERTEX_POINT ( 'NONE', #2548 ) ;
#739=DIRECTION ( 'NONE',  ( 0.000000000000000000, 0.000000000000000000, -1.000000000000000000 ) ) ;
#756=FACE_OUTER_BOUND ( 'NONE', #3119, .T. ) ;
#771=EDGE_CURVE ( 'NONE', #3276, #292, #2717, .T. ) ;
#781=DIRECTION ( 'NONE',  ( 1.000000000000000000, -0.000000000000000000, -0.000000000000000000 ) ) ;
#790=FACE_OUTER_BOUND ( 'NONE', #694, .T. ) ;
#803=ORIENTED_EDGE ( 'NONE', *, *, #6363, .T. ) ;
#850=( NAMED_UNIT ( * ) PLANE_ANGLE_UNIT ( ) SI_UNIT ( $, .RADIAN. ) );
#897=( LENGTH_UNIT ( ) NAMED_UNIT ( * ) SI_UNIT ( .MILLI., .METRE. ) );
#898=ORIENTED_EDGE ( 'NONE', *, *, #8338, .F. ) ;
#927=CIRCLE ( 'NONE', #2364, 1.928074011315806136 ) ;
#997=CARTESIAN_POINT ( 'NONE',  ( 1.299999999999999156, 0.000000000000000000, 1.000000000000000000 ) ) ;
#1010=( NAMED_UNIT ( * ) PLANE_ANGLE_UNIT ( ) SI_UNIT ( $, .RADIAN. ) );
#1058=DIRECTION ( 'NONE',  ( -0.000000000000000000, 1.000000000000000000, 1.224646799147353207E-16 ) ) ;
#1085=MECHANICAL_DESIGN_GEOMETRIC_PRESENTATION_REPRESENTATION('',(#8755),#4269);
#1106=ADVANCED_FACE ( 'NONE', ( #4968 ), #3304, .T. ) ;
#1141=ORIENTED_EDGE ( 'NONE', *, *, #1332, .F. ) ;
#1150=DIRECTION ( 'NONE',  ( 0.000000000000000000, -1.000000000000000000, 0.000000000000000000 ) ) ;
#1179=VERTEX_POINT ( 'NONE', #1972 ) ;
#1222=ORIENTED_EDGE ( 'NONE', *, *, #4211, .F. ) ;
#1312=DIRECTION ( 'NONE',  ( 0.000000000000000000, 0.000000000000000000, 1.000000000000000000 ) ) ;
#1332=EDGE_CURVE ( 'NONE', #1179, #3194, #927, .T. ) ;
#1345=DIRECTION ( 'NONE',  ( -0.000000000000000000, 0.000000000000000000, 1.000000000000000000 ) ) ;
#1376=CARTESIAN_POINT ( 'NONE',  ( 11.30000000000000426, 0.000000000000000000, 1.000000000000000000 ) ) ;
#1385=AXIS2_PLACEMENT_3D ( 'NONE', #7652, #1150, #7993 ) ;
#1411=ORIENTED_EDGE ( 'NONE', *, *, #9974, .F. ) ;
#1414=CIRCLE ( 'NONE', #10446, 1.934182851860891672 ) ;
#1418=ORIENTED_EDGE ( 'NONE', *, *, #771, .F. ) ;
#1419=PLANE ( 'NONE',  #8329 ) ;
#1431=MECHANICAL_DESIGN_GEOMETRIC_PRESENTATION_REPRESENTATION('',(#4072),#10650);
#1453=AXIS2_PLACEMENT_3D ( 'NONE', #1634, #2311, #10752 ) ;
#1473=CARTESIAN_POINT ( 'NONE',  ( 0.5999999999999999778, 0.000000000000000000, 0.000000000000000000 ) ) ;
#1478=ORIENTED_EDGE ( 'NONE', *, *, #4677, .F. ) ;
#1546=AXIS2_PLACEMENT_3D ( 'NONE', #2475, #10760, #7484 ) ;
#1553=ORIENTED_EDGE ( 'NONE', *, *, #8136, .F. ) ;
#1571=CARTESIAN_POINT ( 'NONE',  ( 3.489067535589073648E-18, 0.000000000000000000, 0.000000000000000000 ) ) ;
#1589=VECTOR ( 'NONE', #2536, 1000.000000000000000 ) ;
#1591=COLOUR_RGB ( '',1.000000000000000000, 0.9490196078431372140, 0.9098039215686274384 ) ;
#1610=EDGE_CURVE ( 'NONE', #8468, #3410, #8114, .T. ) ;
#1631=EDGE_CURVE ( 'NONE', #6280, #8297, #4850, .T. ) ;
#1634=CARTESIAN_POINT ( 'NONE',  ( 11.30000000000000426, 0.000000000000000000, 0.000000000000000000 ) ) ;
#1635=ORIENTED_EDGE ( 'NONE', *, *, #4924, .T. ) ;
#1642=AXIS2_PLACEMENT_3D ( 'NONE', #9279, #5885, #8442 ) ;
#1684=CARTESIAN_POINT ( 'NONE',  ( 0.5000000000000000000, 0.2499999999999998335, -1.911797424705720116 ) ) ;
#1706=DIRECTION ( 'NONE',  ( 1.000000000000000000, 0.000000000000000000, 0.000000000000000000 ) ) ;
#1743=SURFACE_STYLE_USAGE ( .BOTH. , #5225 ) ;
#1763=AXIS2_PLACEMENT_3D ( 'NONE', #7594, #7880, #6092 ) ;
#1766=ORIENTED_EDGE ( 'NONE', *, *, #9423, .F. ) ;
#1771=DIRECTION ( 'NONE',  ( -1.000000000000000000, -0.000000000000000000, -0.000000000000000000 ) ) ;
#1886=EDGE_LOOP ( 'NONE', ( #1411, #9822 ) ) ;
#1895=CARTESIAN_POINT ( 'NONE',  ( 0.2309188673393136881, 0.2499999999999998890, 1.812888087824517491 ) ) ;
#1917=DIRECTION ( 'NONE',  ( 0.000000000000000000, -1.084202172485504434E-16, 1.000000000000000000 ) ) ;
#1935=APPLICATION_CONTEXT ( 'automotive_design' ) ;
#1953=CARTESIAN_POINT ( 'NONE',  ( -5.895349312889930360E-16, 0.2499999999999998890, 1.454823465665887605 ) ) ;
#1972=CARTESIAN_POINT ( 'NONE',  ( 0.5000000000000000000, 0.000000000000000000, 1.928074011315806136 ) ) ;
#1996=VERTEX_POINT ( 'NONE', #9898 ) ;
#2014=ORIENTED_EDGE ( 'NONE', *, *, #2239, .F. ) ;
#2030=CARTESIAN_POINT ( 'NONE',  ( -25.39999999999996305, 0.000000000000000000, 0.000000000000000000 ) ) ;
#2149=ORIENTED_EDGE ( 'NONE', *, *, #4021, .T. ) ;
#2174=CARTESIAN_POINT ( 'NONE',  ( 3.489067535589073648E-18, 0.000000000000000000, 0.000000000000000000 ) ) ;
#2201=CARTESIAN_POINT ( 'NONE',  ( 0.5477065543514035850, 0.000000000000000000, 0.000000000000000000 ) ) ;
#2239=EDGE_CURVE ( 'NONE', #6280, #3475, #9824, .T. ) ;
#2250=DIRECTION ( 'NONE',  ( -1.000000000000000000, -0.000000000000000000, -0.000000000000000000 ) ) ;
#2271=ADVANCED_FACE ( 'NONE', ( #3746 ), #10579, .T. ) ;
#2307=AXIS2_PLACEMENT_3D ( 'NONE', #5193, #3646, #1706 ) ;
#2311=DIRECTION ( 'NONE',  ( -1.000000000000000000, -0.000000000000000000, -0.000000000000000000 ) ) ;
#2364=AXIS2_PLACEMENT_3D ( 'NONE', #5632, #3863, #8096 ) ;
#2394=DIRECTION ( 'NONE',  ( 1.000000000000000000, 0.000000000000000000, 0.000000000000000000 ) ) ;
#2400=FACE_OUTER_BOUND ( 'NONE', #5072, .T. ) ;
#2475=CARTESIAN_POINT ( 'NONE',  ( 0.000000000000000000, 0.000000000000000000, 0.000000000000000000 ) ) ;
#2495=ORIENTED_EDGE ( 'NONE', *, *, #4924, .F. ) ;
#2536=DIRECTION ( 'NONE',  ( 0.9961946980917455452, 0.000000000000000000, -0.08715574274765831853 ) ) ;
#2548=CARTESIAN_POINT ( 'NONE',  ( 1.299999999999999156, 1.224646799147353207E-16, -1.000000000000000000 ) ) ;
#2558=ADVANCED_BREP_SHAPE_REPRESENTATION ( '', ( #4773, #2307 ), #6215 ) ;
#2629=B_SPLINE_CURVE_WITH_KNOTS ( 'NONE', 3,
 ( #8617, #279, #1895, #2846, #1953, #10504 ),
 .UNSPECIFIED., .F., .F.,
 ( 4, 2, 4 ),
 ( 0.002363858439908545286, 0.002786031303543299881, 0.003208204167178054476 ),
 .UNSPECIFIED. ) ;
#2664=CARTESIAN_POINT ( 'NONE',  ( -25.39999999999996305, 0.000000000000000000, 1.000000000000000000 ) ) ;
#2706=CARTESIAN_POINT ( 'NONE',  ( 1.299999999999999156, 2.449293598294706907E-16, 2.000000000000000000 ) ) ;
#2717=LINE ( 'NONE', #2664, #7849 ) ;
#2723=FACE_OUTER_BOUND ( 'NONE', #2910, .T. ) ;
#2741=EDGE_LOOP ( 'NONE', ( #7713, #2014, #10651, #2858, #898, #271, #7934, #2149 ) ) ;
#2769=ADVANCED_FACE ( 'NONE', ( #8955 ), #8899, .T. ) ;
#2799=( NAMED_UNIT ( * ) SI_UNIT ( $, .STERADIAN. ) SOLID_ANGLE_UNIT ( ) );
#2820=AXIS2_PLACEMENT_3D ( 'NONE', #3839, #6229, #4493 ) ;
#2846=CARTESIAN_POINT ( 'NONE',  ( 0.05007509226404534275, 0.2499999999999998335, 1.595201548406556036 ) ) ;
#2858=ORIENTED_EDGE ( 'NONE', *, *, #1332, .T. ) ;
#2910=EDGE_LOOP ( 'NONE', ( #3732, #5460, #8389, #1222 ) ) ;
#2937=VERTEX_POINT ( 'NONE', #8232 ) ;
#2984=ORIENTED_EDGE ( 'NONE', *, *, #7638, .T. ) ;
#2990=ORIENTED_EDGE ( 'NONE', *, *, #1631, .F. ) ;
#2998=DIRECTION ( 'NONE',  ( 0.000000000000000000, -1.084202172485504434E-16, 1.000000000000000000 ) ) ;
#3007=CARTESIAN_POINT ( 'NONE',  ( 0.5000000000000000000, 0.000000000000000000, 0.000000000000000000 ) ) ;
#3029=PRODUCT_CONTEXT ( 'NONE', #1935, 'mechanical' ) ;
#3046=ORIENTED_EDGE ( 'NONE', *, *, #7638, .F. ) ;
#3053=CIRCLE ( 'NONE', #1453, 1.000000000000000000 ) ;
#3098=CARTESIAN_POINT ( 'NONE',  ( 0.5000000000000000000, 2.361209666477099964E-16, -1.928074011315806136 ) ) ;
#3119=EDGE_LOOP ( 'NONE', ( #9591, #7980, #8165, #6395 ) ) ;
#3188=AXIS2_PLACEMENT_3D ( 'NONE', #1571, #10797, #8356 ) ;
#3194=VERTEX_POINT ( 'NONE', #9649 ) ;
#3203=ORIENTED_EDGE ( 'NONE', *, *, #2239, .T. ) ;
#3246=PRODUCT_DEFINITION_SHAPE ( 'NONE', 'NONE',  #5895 ) ;
#3276=VERTEX_POINT ( 'NONE', #1376 ) ;
#3304=CYLINDRICAL_SURFACE ( 'NONE', #8558, 1.000000000000000000 ) ;
#3310=CARTESIAN_POINT ( 'NONE',  ( 0.000000000000000000, 0.000000000000000000, -1.886264737416298631 ) ) ;
#3335=CIRCLE ( 'NONE', #520, 1.000000000000000000 ) ;
#3339=CARTESIAN_POINT ( 'NONE',  ( 0.3608130681495587133, 0.2499999999999998890, -1.888070236890894815 ) ) ;
#3340=CIRCLE ( 'NONE', #7605, 1.928074011315806136 ) ;
#3352=DIRECTION ( 'NONE',  ( 0.000000000000000000, 0.000000000000000000, 1.000000000000000000 ) ) ;
#3362=CARTESIAN_POINT ( 'NONE',  ( 1.299999999999999156, 0.000000000000000000, -2.000000000000000000 ) ) ;
#3379=PLANE ( 'NONE',  #1642 ) ;
#3405=AXIS2_PLACEMENT_3D ( 'NONE', #3007, #6396, #8174 ) ;
#3410=VERTEX_POINT ( 'NONE', #6958 ) ;
#3475=VERTEX_POINT ( 'NONE', #10622 ) ;
#3491=DIRECTION ( 'NONE',  ( 0.000000000000000000, 1.000000000000000000, 0.000000000000000000 ) ) ;
#3507=( NAMED_UNIT ( * ) SI_UNIT ( $, .STERADIAN. ) SOLID_ANGLE_UNIT ( ) );
#3525=AXIS2_PLACEMENT_3D ( 'NONE', #8671, #8790, #10444 ) ;
#3646=DIRECTION ( 'NONE',  ( 0.000000000000000000, 0.000000000000000000, 1.000000000000000000 ) ) ;
#3713=DIRECTION ( 'NONE',  ( -1.000000000000000000, -0.000000000000000000, -0.000000000000000000 ) ) ;
#3722=DIRECTION ( 'NONE',  ( 0.000000000000000000, 0.000000000000000000, 1.000000000000000000 ) ) ;
#3732=ORIENTED_EDGE ( 'NONE', *, *, #7187, .T. ) ;
#3746=FACE_OUTER_BOUND ( 'NONE', #615, .T. ) ;
#3839=CARTESIAN_POINT ( 'NONE',  ( 1.299999999999999156, 0.000000000000000000, 0.000000000000000000 ) ) ;
#3863=DIRECTION ( 'NONE',  ( 1.000000000000000000, -0.000000000000000000, -0.000000000000000000 ) ) ;
#3874=ADVANCED_FACE ( 'NONE', ( #2723 ), #3379, .F. ) ;
#3882=CIRCLE ( 'NONE', #8483, 1.928074011315806136 ) ;
#3885=VECTOR ( 'NONE', #2998, 1000.000000000000000 ) ;
#3965=PLANE ( 'NONE',  #9538 ) ;
#3985=CARTESIAN_POINT ( 'NONE',  ( 0.3600944671415647336, -0.2500000000000001665, 1.887947737020719163 ) ) ;
#4021=EDGE_CURVE ( 'NONE', #8978, #8323, #8219, .T. ) ;
#4037=CARTESIAN_POINT ( 'NONE',  ( 0.000000000000000000, 0.000000000000000000, 0.000000000000000000 ) ) ;
#4072=STYLED_ITEM ( 'NONE', ( #8631 ), #2558 ) ;
#4088=ORIENTED_EDGE ( 'NONE', *, *, #1610, .T. ) ;
#4113=FACE_OUTER_BOUND ( 'NONE', #7569, .T. ) ;
#4165=DIRECTION ( 'NONE',  ( 0.000000000000000000, 0.000000000000000000, 1.000000000000000000 ) ) ;
#4190=FACE_OUTER_BOUND ( 'NONE', #2741, .T. ) ;
#4191=APPLICATION_CONTEXT ( 'automotive_design' ) ;
#4197=AXIS2_PLACEMENT_3D ( 'NONE', #8886, #7996, #6444 ) ;
#4211=EDGE_CURVE ( 'NONE', #8978, #3194, #4522, .T. ) ;
#4269=( GEOMETRIC_REPRESENTATION_CONTEXT ( 3 ) GLOBAL_UNCERTAINTY_ASSIGNED_CONTEXT ( ( #9164 ) ) GLOBAL_UNIT_ASSIGNED_CONTEXT ( ( #897, #7743, #3507 ) ) REPRESENTATION_CONTEXT ( 'NONE', 'WORKASPACE' ) );
#4318=DIRECTION ( 'NONE',  ( 0.000000000000000000, -0.000000000000000000, 1.000000000000000000 ) ) ;
#4440=DIRECTION ( 'NONE',  ( 1.000000000000000000, -0.000000000000000000, -0.000000000000000000 ) ) ;
#4479=VECTOR ( 'NONE', #1917, 1000.000000000000000 ) ;
#4493=DIRECTION ( 'NONE',  ( 0.000000000000000000, 0.000000000000000000, 1.000000000000000000 ) ) ;
#4522=LINE ( 'NONE', #5234, #4479 ) ;
#4523=ORIENTED_EDGE ( 'NONE', *, *, #5916, .F. ) ;
#4550=LINE ( 'NONE', #7957, #9752 ) ;
#4597=CIRCLE ( 'NONE', #10645, 0.5999999999999999778 ) ;
#4614=DIRECTION ( 'NONE',  ( 0.000000000000000000, 0.000000000000000000, -1.000000000000000000 ) ) ;
#4649=LINE ( 'NONE', #9879, #130 ) ;
#4650=EDGE_LOOP ( 'NONE', ( #8170, #10143, #6825, #7130 ) ) ;
#4653=LINE ( 'NONE', #8060, #3885 ) ;
#4677=EDGE_CURVE ( 'NONE', #3276, #8026, #3053, .T. ) ;
#4753=CARTESIAN_POINT ( 'NONE',  ( 0.2307700686259116507, -0.2500000000000000555, 1.812750528907548730 ) ) ;
#4773=MANIFOLD_SOLID_BREP ( 'Slot', #7842 ) ;
#4848=DIRECTION ( 'NONE',  ( -1.000000000000000000, -0.000000000000000000, -0.000000000000000000 ) ) ;
#4850=LINE ( 'NONE', #8257, #5546 ) ;
#4869=ORIENTED_EDGE ( 'NONE', *, *, #1610, .F. ) ;
#4915=ORIENTED_EDGE ( 'NONE', *, *, #5750, .F. ) ;
#4919=CIRCLE ( 'NONE', #1385, 0.5999999999999999778 ) ;
#4924=EDGE_CURVE ( 'NONE', #8323, #3410, #3882, .T. ) ;
#4935=ORIENTED_EDGE ( 'NONE', *, *, #8501, .T. ) ;
#4955=PLANE ( 'NONE',  #3188 ) ;
#4956=CARTESIAN_POINT ( 'NONE',  ( 0.2300425840023376800, 0.2499999999999998335, -1.812072026511089229 ) ) ;
#4968=FACE_OUTER_BOUND ( 'NONE', #4650, .T. ) ;
#5051=CARTESIAN_POINT ( 'NONE',  ( 1.299999999999999156, 0.000000000000000000, 0.000000000000000000 ) ) ;
#5072=EDGE_LOOP ( 'NONE', ( #6097, #4935 ) ) ;
#5193=CARTESIAN_POINT ( 'NONE',  ( 0.000000000000000000, 0.000000000000000000, 0.000000000000000000 ) ) ;
#5209=PLANE ( 'NONE',  #5645 ) ;
#5225=SURFACE_SIDE_STYLE ('',( #8466 ) ) ;
#5234=CARTESIAN_POINT ( 'NONE',  ( 0.5000000000000000000, -0.2499999999999997224, -2.000000000000000000 ) ) ;
#5265=FACE_BOUND ( 'NONE', #10925, .T. ) ;
#5380=CARTESIAN_POINT ( 'NONE',  ( 1.299999999999999156, 0.000000000000000000, 0.000000000000000000 ) ) ;
#5420=CARTESIAN_POINT ( 'NONE',  ( 0.000000000000000000, 0.2499999999999998335, -1.312875263449799101 ) ) ;
#5424=DIRECTION ( 'NONE',  ( -1.000000000000000000, -0.000000000000000000, -0.000000000000000000 ) ) ;
#5460=ORIENTED_EDGE ( 'NONE', *, *, #9974, .T. ) ;
#5464=VECTOR ( 'NONE', #7770, 1000.000000000000000 ) ;
#5483=TOROIDAL_SURFACE ( 'NONE', #6915, 1.336466033005844434, 0.5999999999999999778 ) ;
#5546=VECTOR ( 'NONE', #10115, 1000.000000000000000 ) ;
#5547=DIRECTION ( 'NONE',  ( 0.000000000000000000, 0.000000000000000000, -1.000000000000000000 ) ) ;
#5558=AXIS2_PLACEMENT_3D ( 'NONE', #2030, #2250, #9636 ) ;
#5632=CARTESIAN_POINT ( 'NONE',  ( 0.5000000000000000000, 0.000000000000000000, 0.000000000000000000 ) ) ;
#5645=AXIS2_PLACEMENT_3D ( 'NONE', #6732, #3491, #4318 ) ;
#5646=CARTESIAN_POINT ( 'NONE',  ( 0.5000000000000000000, -0.2500000000000001665, 1.911797424705720116 ) ) ;
#5721=EDGE_LOOP ( 'NONE', ( #2990, #3203, #803, #2984 ) ) ;
#5732=CARTESIAN_POINT ( 'NONE',  ( 0.5000000000000000000, 0.2499999999999998335, -2.000000000000000000 ) ) ;
#5750=EDGE_CURVE ( 'NONE', #292, #724, #8668, .T. ) ;
#5784=DIRECTION ( 'NONE',  ( 0.000000000000000000, 0.000000000000000000, 1.000000000000000000 ) ) ;
#5790=ORIENTED_EDGE ( 'NONE', *, *, #8531, .T. ) ;
#5858=PRODUCT_DEFINITION_FORMATION_WITH_SPECIFIED_SOURCE ( 'ANY', '', #10959, .NOT_KNOWN. ) ;
#5885=DIRECTION ( 'NONE',  ( 0.000000000000000000, -1.000000000000000000, -1.084202172485504434E-16 ) ) ;
#5895=PRODUCT_DEFINITION ( 'UNKNOWN', '', #5858, #9261 ) ;
#5916=EDGE_CURVE ( 'NONE', #1996, #1179, #3340, .T. ) ;
#5946=EDGE_CURVE ( 'NONE', #1996, #2937, #2629, .T. ) ;
#6029=ADVANCED_FACE ( 'NONE', ( #227, #5265 ), #169, .F. ) ;
#6039=EDGE_CURVE ( 'NONE', #2937, #8468, #4550, .T. ) ;
#6073=( LENGTH_UNIT ( ) NAMED_UNIT ( * ) SI_UNIT ( .MILLI., .METRE. ) );
#6092=DIRECTION ( 'NONE',  ( 0.000000000000000000, 0.000000000000000000, 1.000000000000000000 ) ) ;
#6097=ORIENTED_EDGE ( 'NONE', *, *, #6039, .F. ) ;
#6117=ORIENTED_EDGE ( 'NONE', *, *, #5750, .T. ) ;
#6130=FILL_AREA_STYLE_COLOUR ( '', #1591 ) ;
#6171=CARTESIAN_POINT ( 'NONE',  ( 0.5000000000000000000, 0.000000000000000000, 0.000000000000000000 ) ) ;
#6176=CARTESIAN_POINT ( 'NONE',  ( 0.5000000000000000000, -0.2499999999999997224, -1.911797424705720116 ) ) ;
#6215=( GEOMETRIC_REPRESENTATION_CONTEXT ( 3 ) GLOBAL_UNCERTAINTY_ASSIGNED_CONTEXT ( ( #8067 ) ) GLOBAL_UNIT_ASSIGNED_CONTEXT ( ( #6073, #1010, #2799 ) ) REPRESENTATION_CONTEXT ( 'NONE', 'WORKASPACE' ) );
#6229=DIRECTION ( 'NONE',  ( -1.000000000000000000, -0.000000000000000000, -0.000000000000000000 ) ) ;
#6238=CARTESIAN_POINT ( 'NONE',  ( 0.04978537780227581394, -0.2499999999999997780, -1.594765474869574540 ) ) ;
#6280=VERTEX_POINT ( 'NONE', #10922 ) ;
#6362=ORIENTED_EDGE ( 'NONE', *, *, #5946, .T. ) ;
#6363=EDGE_CURVE ( 'NONE', #3475, #10242, #10243, .T. ) ;
#6395=ORIENTED_EDGE ( 'NONE', *, *, #6363, .F. ) ;
#6396=DIRECTION ( 'NONE',  ( 1.000000000000000000, -0.000000000000000000, -0.000000000000000000 ) ) ;
#6444=DIRECTION ( 'NONE',  ( 0.000000000000000000, 0.000000000000000000, 1.000000000000000000 ) ) ;
#6448=ADVANCED_FACE ( 'NONE', ( #4190 ), #9566, .T. ) ;
#6482=ORIENTED_EDGE ( 'NONE', *, *, #8531, .F. ) ;
#6632=DIRECTION ( 'NONE',  ( 0.000000000000000000, 0.000000000000000000, 1.000000000000000000 ) ) ;
#6672=ORIENTED_EDGE ( 'NONE', *, *, #6039, .T. ) ;
#6686=VERTEX_POINT ( 'NONE', #7363 ) ;
#6687=CARTESIAN_POINT ( 'NONE',  ( 11.30000000000000071, 1.000000000000000000, 0.000000000000000000 ) ) ;
#6724=ADVANCED_FACE ( 'NONE', ( #2400 ), #4955, .T. ) ;
#6732=CARTESIAN_POINT ( 'NONE',  ( 0.5000000000000000000, 0.2499999999999998335, 2.000000000000000000 ) ) ;
#6743=ADVANCED_FACE ( 'NONE', ( #790 ), #1419, .T. ) ;
#6823=ADVANCED_FACE ( 'NONE', ( #9028 ), #5483, .T. ) ;
#6825=ORIENTED_EDGE ( 'NONE', *, *, #771, .T. ) ;
#6887=CIRCLE ( 'NONE', #10432, 1.336466033005844434 ) ;
#6915=AXIS2_PLACEMENT_3D ( 'NONE', #1473, #4848, #8256 ) ;
#6918=ORIENTED_EDGE ( 'NONE', *, *, #9343, .F. ) ;
#6935=ORIENTED_EDGE ( 'NONE', *, *, #5946, .F. ) ;
#6942=EDGE_CURVE ( 'NONE', #3475, #8323, #4597, .T. ) ;
#6958=CARTESIAN_POINT ( 'NONE',  ( 0.5000000000000000000, 0.2499999999999998335, -1.911797424705720116 ) ) ;
#6966=( LENGTH_UNIT ( ) NAMED_UNIT ( * ) SI_UNIT ( .MILLI., .METRE. ) );
#7120=DIRECTION ( 'NONE',  ( 0.000000000000000000, 0.000000000000000000, 1.000000000000000000 ) ) ;
#7124=DIRECTION ( 'NONE',  ( 0.000000000000000000, -6.217248937900875838E-15, 1.000000000000000000 ) ) ;
#7130=ORIENTED_EDGE ( 'NONE', *, *, #9373, .F. ) ;
#7187=EDGE_CURVE ( 'NONE', #8978, #8454, #8440, .T. ) ;
#7206=ORIENTED_EDGE ( 'NONE', *, *, #9373, .T. ) ;
#7212=CARTESIAN_POINT ( 'NONE',  ( 0.05007909176323183803, -0.2500000000000001665, 1.595164775286566305 ) ) ;
#7284=UNCERTAINTY_MEASURE_WITH_UNIT (LENGTH_MEASURE( 1.000000000000000082E-05 ), #6966, 'distance_accuracy_value', 'NONE');
#7363=CARTESIAN_POINT ( 'NONE',  ( 0.000000000000000000, -0.2500000000000001110, 1.312875263449798879 ) ) ;
#7418=CONICAL_SURFACE ( 'NONE', #1546, 1.886264737416298631, 0.08726646259971662656 ) ;
#7462=DIRECTION ( 'NONE',  ( -1.000000000000000000, 0.000000000000000000, 0.000000000000000000 ) ) ;
#7484=DIRECTION ( 'NONE',  ( 0.000000000000000000, 0.000000000000000000, -1.000000000000000000 ) ) ;
#7547=ORIENTED_EDGE ( 'NONE', *, *, #10541, .F. ) ;
#7562=FACE_OUTER_BOUND ( 'NONE', #8424, .T. ) ;
#7569=EDGE_LOOP ( 'NONE', ( #587, #1141, #4523, #5790, #2495, #8793 ) ) ;
#7570=DIRECTION ( 'NONE',  ( 0.000000000000000000, -1.224646799147352961E-16, 1.000000000000000000 ) ) ;
#7594=CARTESIAN_POINT ( 'NONE',  ( 0.5999999999999999778, 0.000000000000000000, 0.000000000000000000 ) ) ;
#7605=AXIS2_PLACEMENT_3D ( 'NONE', #6171, #4440, #7124 ) ;
#7628=CONICAL_SURFACE ( 'NONE', #8176, 1.886264737416298631, 0.08726646259971662656 ) ;
#7637=( NAMED_UNIT ( * ) SI_UNIT ( $, .STERADIAN. ) SOLID_ANGLE_UNIT ( ) );
#7638=EDGE_CURVE ( 'NONE', #10242, #8297, #10654, .T. ) ;
#7652=CARTESIAN_POINT ( 'NONE',  ( 0.5999999999999999778, 0.000000000000000000, 1.336466033005844434 ) ) ;
#7692=AXIS2_PLACEMENT_3D ( 'NONE', #2201, #423, #1312 ) ;
#7713=ORIENTED_EDGE ( 'NONE', *, *, #6942, .F. ) ;
#7743=( NAMED_UNIT ( * ) PLANE_ANGLE_UNIT ( ) SI_UNIT ( $, .RADIAN. ) );
#7770=DIRECTION ( 'NONE',  ( -1.000000000000000000, -0.000000000000000000, -0.000000000000000000 ) ) ;
#7807=ADVANCED_FACE ( 'NONE', ( #10822 ), #7628, .T. ) ;
#7842=CLOSED_SHELL ( 'NONE', ( #6823, #8569, #2271, #6724, #1106, #6743, #2769, #7807, #6029, #6448, #9197, #3874, #9022 ) ) ;
#7846=CARTESIAN_POINT ( 'NONE',  ( 0.2309054577385449836, -0.2499999999999997780, -1.812959136724909603 ) ) ;
#7849=VECTOR ( 'NONE', #1771, 1000.000000000000000 ) ;
#7880=DIRECTION ( 'NONE',  ( -1.000000000000000000, -0.000000000000000000, -0.000000000000000000 ) ) ;
#7881=AXIS2_PLACEMENT_3D ( 'NONE', #2174, #453, #1345 ) ;
#7934=ORIENTED_EDGE ( 'NONE', *, *, #7187, .F. ) ;
#7940=LINE ( 'NONE', #8891, #5464 ) ;
#7952=DIRECTION ( 'NONE',  ( -1.000000000000000000, -0.000000000000000000, -0.000000000000000000 ) ) ;
#7957=CARTESIAN_POINT ( 'NONE',  ( 0.000000000000000000, 0.2499999999999998335, 2.000000000000000000 ) ) ;
#7980=ORIENTED_EDGE ( 'NONE', *, *, #1631, .T. ) ;
#7993=DIRECTION ( 'NONE',  ( 0.000000000000000000, 0.000000000000000000, -1.000000000000000000 ) ) ;
#7996=DIRECTION ( 'NONE',  ( -1.000000000000000000, -0.000000000000000000, -0.000000000000000000 ) ) ;
#8026=VERTEX_POINT ( 'NONE', #90 ) ;
#8036=ORIENTED_EDGE ( 'NONE', *, *, #5916, .T. ) ;
#8060=CARTESIAN_POINT ( 'NONE',  ( 0.000000000000000000, -0.2499999999999997224, -2.000000000000000000 ) ) ;
#8067=UNCERTAINTY_MEASURE_WITH_UNIT (LENGTH_MEASURE( 1.000000000000000082E-05 ), #6073, 'distance_accuracy_value', 'NONE');
#8096=DIRECTION ( 'NONE',  ( 0.000000000000000000, 0.000000000000000000, 1.000000000000000000 ) ) ;
#8114=B_SPLINE_CURVE_WITH_KNOTS ( 'NONE', 3,
 ( #10950, #9136, #9243, #4956, #3339, #1684 ),
 .UNSPECIFIED., .F., .F.,
 ( 4, 2, 4 ),
 ( 0.003191392849877886743, 0.003612977948258624256, 0.004034563046639362202 ),
 .UNSPECIFIED. ) ;
#8136=EDGE_CURVE ( 'NONE', #6280, #1179, #4919, .T. ) ;
#8163=CARTESIAN_POINT ( 'NONE',  ( 0.000000000000000000, -0.2499999999999997780, -1.312875263449798879 ) ) ;
#8165=ORIENTED_EDGE ( 'NONE', *, *, #9343, .T. ) ;
#8170=ORIENTED_EDGE ( 'NONE', *, *, #9835, .F. ) ;
#8174=DIRECTION ( 'NONE',  ( 0.000000000000000000, 1.065814103640150121E-14, 1.000000000000000000 ) ) ;
#8176=AXIS2_PLACEMENT_3D ( 'NONE', #4037, #8226, #5547 ) ;
#8219=CIRCLE ( 'NONE', #3405, 1.928074011315806136 ) ;
#8226=DIRECTION ( 'NONE',  ( 1.000000000000000000, 0.000000000000000000, 0.000000000000000000 ) ) ;
#8232=CARTESIAN_POINT ( 'NONE',  ( 0.000000000000000000, 0.2499999999999998335, 1.312875263449799101 ) ) ;
#8246=DIRECTION ( 'NONE',  ( 0.000000000000000000, 0.000000000000000000, 1.000000000000000000 ) ) ;
#8256=DIRECTION ( 'NONE',  ( 0.000000000000000000, 0.000000000000000000, 1.000000000000000000 ) ) ;
#8257=CARTESIAN_POINT ( 'NONE',  ( 0.000000000000000000, 2.310008073021392973E-16, 1.886264737416298631 ) ) ;
#8297=VERTEX_POINT ( 'NONE', #2706 ) ;
#8323=VERTEX_POINT ( 'NONE', #3098 ) ;
#8329=AXIS2_PLACEMENT_3D ( 'NONE', #6687, #588, #739 ) ;
#8338=EDGE_CURVE ( 'NONE', #6686, #3194, #215, .T. ) ;
#8356=DIRECTION ( 'NONE',  ( -0.000000000000000000, 0.000000000000000000, 1.000000000000000000 ) ) ;
#8368=CARTESIAN_POINT ( 'NONE',  ( -25.39999999999996305, 0.000000000000000000, 0.000000000000000000 ) ) ;
#8389=ORIENTED_EDGE ( 'NONE', *, *, #8338, .T. ) ;
#8424=EDGE_LOOP ( 'NONE', ( #4088, #6482, #6362, #6672 ) ) ;
#8440=B_SPLINE_CURVE_WITH_KNOTS ( 'NONE', 3,
 ( #6176, #344, #7846, #6238, #9622, #8794 ),
 .UNSPECIFIED., .F., .F.,
 ( 4, 2, 4 ),
 ( 0.003549988921687060022, 0.003971677118101640293, 0.004393365314516220997 ),
 .UNSPECIFIED. ) ;
#8442=DIRECTION ( 'NONE',  ( 0.000000000000000000, 1.084202172485504434E-16, -1.000000000000000000 ) ) ;
#8454=VERTEX_POINT ( 'NONE', #8163 ) ;
#8466=SURFACE_STYLE_FILL_AREA ( #8579 ) ;
#8468=VERTEX_POINT ( 'NONE', #5420 ) ;
#8483=AXIS2_PLACEMENT_3D ( 'NONE', #9174, #781, #8246 ) ;
#8489=AXIS2_PLACEMENT_3D ( 'NONE', #5051, #60, #4165 ) ;
#8501=EDGE_CURVE ( 'NONE', #2937, #8468, #10779, .T. ) ;
#8531=EDGE_CURVE ( 'NONE', #1996, #3410, #4649, .T. ) ;
#8558=AXIS2_PLACEMENT_3D ( 'NONE', #8368, #25, #3352 ) ;
#8569=ADVANCED_FACE ( 'NONE', ( #756 ), #7418, .T. ) ;
#8579=FILL_AREA_STYLE ('',( #6130 ) ) ;
#8617=CARTESIAN_POINT ( 'NONE',  ( 0.5000000000000000000, 0.2499999999999998335, 1.911797424705720116 ) ) ;
#8631=PRESENTATION_STYLE_ASSIGNMENT (( #1743 ) ) ;
#8668=CIRCLE ( 'NONE', #8489, 1.000000000000000000 ) ;
#8671=CARTESIAN_POINT ( 'NONE',  ( 1.299999999999999600, 1.000000000000000000, 0.000000000000000000 ) ) ;
#8677=CARTESIAN_POINT ( 'NONE',  ( 0.5999999999999999778, 1.636698849489768475E-16, -1.336466033005844434 ) ) ;
#8691=AXIS2_PLACEMENT_3D ( 'NONE', #387, #3713, #449 ) ;
#8755=STYLED_ITEM('',(#11027),#4773);
#8790=DIRECTION ( 'NONE',  ( -1.000000000000000000, 0.000000000000000000, -0.000000000000000000 ) ) ;
#8793=ORIENTED_EDGE ( 'NONE', *, *, #4021, .F. ) ;
#8794=CARTESIAN_POINT ( 'NONE',  ( 0.000000000000000000, -0.2499999999999997780, -1.312875263449798879 ) ) ;
#8867=SHAPE_REPRESENTATION ( 'slotted pan head screw_iso_ISO 1580 - M2 x 10 - 10N', ( #2307 ), #6215 ) ;
#8886=CARTESIAN_POINT ( 'NONE',  ( 0.000000000000000000, 0.000000000000000000, 0.000000000000000000 ) ) ;
#8891=CARTESIAN_POINT ( 'NONE',  ( -25.39999999999996305, 1.224646799147353207E-16, -1.000000000000000000 ) ) ;
#8899=PLANE ( 'NONE',  #7881 ) ;
#8955=FACE_OUTER_BOUND ( 'NONE', #1886, .T. ) ;
#8978=VERTEX_POINT ( 'NONE', #9126 ) ;
#8988=CARTESIAN_POINT ( 'NONE',  ( -9.277551871276348458E-15, -0.2500000000000001110, 1.454152683131083812 ) ) ;
#9022=ADVANCED_FACE ( 'NONE', ( #4113 ), #3965, .T. ) ;
#9028=FACE_OUTER_BOUND ( 'NONE', #9750, .T. ) ;
#9032=CIRCLE ( 'NONE', #9201, 1.000000000000000000 ) ;
#9095=DIRECTION ( 'NONE',  ( 0.000000000000000000, 0.000000000000000000, -1.000000000000000000 ) ) ;
#9126=CARTESIAN_POINT ( 'NONE',  ( 0.5000000000000000000, -0.2499999999999997224, -1.911797424705720116 ) ) ;
#9136=CARTESIAN_POINT ( 'NONE',  ( -1.478538361079743326E-14, 0.2499999999999997780, -1.453737367178235651 ) ) ;
#9164=UNCERTAINTY_MEASURE_WITH_UNIT (LENGTH_MEASURE( 1.000000000000000082E-05 ), #897, 'distance_accuracy_value', 'NONE');
#9174=CARTESIAN_POINT ( 'NONE',  ( 0.5000000000000000000, 0.000000000000000000, 0.000000000000000000 ) ) ;
#9197=ADVANCED_FACE ( 'NONE', ( #7562 ), #5209, .F. ) ;
#9201=AXIS2_PLACEMENT_3D ( 'NONE', #9495, #7952, #7120 ) ;
#9243=CARTESIAN_POINT ( 'NONE',  ( 0.05011565059742421196, 0.2499999999999998890, -1.595010514166263382 ) ) ;
#9261=PRODUCT_DEFINITION_CONTEXT ( 'detailed design', #4191, 'design' ) ;
#9279=CARTESIAN_POINT ( 'NONE',  ( 0.5000000000000000000, -0.2499999999999997224, -2.000000000000000000 ) ) ;
#9343=EDGE_CURVE ( 'NONE', #8297, #10242, #10076, .T. ) ;
#9373=EDGE_CURVE ( 'NONE', #724, #292, #3335, .T. ) ;
#9423=EDGE_CURVE ( 'NONE', #8026, #3276, #9032, .T. ) ;
#9495=CARTESIAN_POINT ( 'NONE',  ( 11.30000000000000426, 0.000000000000000000, 0.000000000000000000 ) ) ;
#9525=ORIENTED_EDGE ( 'NONE', *, *, #6942, .T. ) ;
#9538=AXIS2_PLACEMENT_3D ( 'NONE', #5732, #7462, #6632 ) ;
#9566=TOROIDAL_SURFACE ( 'NONE', #1763, 1.336466033005844434, 0.5999999999999999778 ) ;
#9591=ORIENTED_EDGE ( 'NONE', *, *, #10541, .T. ) ;
#9622=CARTESIAN_POINT ( 'NONE',  ( -1.101142831430589948E-16, -0.2499999999999997780, -1.455170506525537366 ) ) ;
#9636=DIRECTION ( 'NONE',  ( 0.000000000000000000, 0.000000000000000000, 1.000000000000000000 ) ) ;
#9637=EDGE_LOOP ( 'NONE', ( #3046, #6918 ) ) ;
#9649=CARTESIAN_POINT ( 'NONE',  ( 0.5000000000000000000, -0.2500000000000001665, 1.911797424705720116 ) ) ;
#9714=DIRECTION ( 'NONE',  ( 0.000000000000000000, 0.000000000000000000, 1.000000000000000000 ) ) ;
#9742=ORIENTED_EDGE ( 'NONE', *, *, #8501, .F. ) ;
#9746=SHAPE_DEFINITION_REPRESENTATION ( #3246, #8867 ) ;
#9750=EDGE_LOOP ( 'NONE', ( #7547, #9525, #1635, #4869, #9742, #6935, #8036, #1553 ) ) ;
#9752=VECTOR ( 'NONE', #4614, 1000.000000000000000 ) ;
#9771=EDGE_CURVE ( 'NONE', #8454, #6686, #6887, .T. ) ;
#9819=CARTESIAN_POINT ( 'NONE',  ( 0.5477065543514035850, 0.000000000000000000, 0.000000000000000000 ) ) ;
#9822=ORIENTED_EDGE ( 'NONE', *, *, #9771, .T. ) ;
#9824=CIRCLE ( 'NONE', #7692, 1.934182851860891672 ) ;
#9835=EDGE_CURVE ( 'NONE', #8026, #724, #7940, .T. ) ;
#9879=CARTESIAN_POINT ( 'NONE',  ( 0.5000000000000000000, 0.2499999999999998335, 2.000000000000000000 ) ) ;
#9898=CARTESIAN_POINT ( 'NONE',  ( 0.5000000000000000000, 0.2499999999999998335, 1.911797424705720116 ) ) ;
#9974=EDGE_CURVE ( 'NONE', #8454, #6686, #4653, .T. ) ;
#10076=CIRCLE ( 'NONE', #2820, 2.000000000000000000 ) ;
#10115=DIRECTION ( 'NONE',  ( 0.9961946980917455452, 1.067350013832299055E-17, 0.08715574274765831853 ) ) ;
#10143=ORIENTED_EDGE ( 'NONE', *, *, #9423, .T. ) ;
#10242=VERTEX_POINT ( 'NONE', #3362 ) ;
#10243=LINE ( 'NONE', #3310, #1589 ) ;
#10432=AXIS2_PLACEMENT_3D ( 'NONE', #322, #5424, #9714 ) ;
#10444=DIRECTION ( 'NONE',  ( -0.000000000000000000, 0.000000000000000000, 1.000000000000000000 ) ) ;
#10446=AXIS2_PLACEMENT_3D ( 'NONE', #9819, #2394, #5784 ) ;
#10504=CARTESIAN_POINT ( 'NONE',  ( 0.000000000000000000, 0.2499999999999998335, 1.312875263449799101 ) ) ;
#10541=EDGE_CURVE ( 'NONE', #3475, #6280, #1414, .T. ) ;
#10579=CYLINDRICAL_SURFACE ( 'NONE', #5558, 1.000000000000000000 ) ;
#10622=CARTESIAN_POINT ( 'NONE',  ( 0.5477065543514035850, 0.000000000000000000, -1.934182851860891672 ) ) ;
#10645=AXIS2_PLACEMENT_3D ( 'NONE', #8677, #1058, #7570 ) ;
#10650=( GEOMETRIC_REPRESENTATION_CONTEXT ( 3 ) GLOBAL_UNCERTAINTY_ASSIGNED_CONTEXT ( ( #7284 ) ) GLOBAL_UNIT_ASSIGNED_CONTEXT ( ( #6966, #850, #7637 ) ) REPRESENTATION_CONTEXT ( 'NONE', 'WORKASPACE' ) );
#10651=ORIENTED_EDGE ( 'NONE', *, *, #8136, .T. ) ;
#10654=CIRCLE ( 'NONE', #8691, 2.000000000000000000 ) ;
#10711=CARTESIAN_POINT ( 'NONE',  ( 0.000000000000000000, -0.2500000000000001110, 1.312875263449798879 ) ) ;
#10752=DIRECTION ( 'NONE',  ( 0.000000000000000000, 0.000000000000000000, 1.000000000000000000 ) ) ;
#10760=DIRECTION ( 'NONE',  ( 1.000000000000000000, 0.000000000000000000, 0.000000000000000000 ) ) ;
#10779=CIRCLE ( 'NONE', #4197, 1.336466033005844434 ) ;
#10797=DIRECTION ( 'NONE',  ( -1.000000000000000000, 0.000000000000000000, -0.000000000000000000 ) ) ;
#10822=FACE_OUTER_BOUND ( 'NONE', #5721, .T. ) ;
#10922=CARTESIAN_POINT ( 'NONE',  ( 0.5477065543514035850, 2.408992218395923449E-16, 1.934182851860891672 ) ) ;
#10925=EDGE_LOOP ( 'NONE', ( #6117, #7206 ) ) ;
#10950=CARTESIAN_POINT ( 'NONE',  ( 0.000000000000000000, 0.2499999999999998335, -1.312875263449799101 ) ) ;
#10959=PRODUCT ( 'slotted pan head screw_iso_ISO 1580 - M2 x 10 - 10N', 'slotted pan head screw_iso_ISO 1580 - M2 x 10 - 10N', '', ( #3029 ) ) ;
#11021=COLOUR_RGB('Black',0.12,0.14,0.17);
#11022=FILL_AREA_STYLE_COLOUR('',#11021);
#11023=FILL_AREA_STYLE('',(#11022));
#11024=SURFACE_STYLE_FILL_AREA(#11023);
#11025=SURFACE_SIDE_STYLE('',(#11024));
#11026=SURFACE_STYLE_USAGE(.BOTH.,#11025);
#11027=PRESENTATION_STYLE_ASSIGNMENT((#11026));
ENDSEC;
END-ISO-10303-21;
